ISO-10303-21;
HEADER;
/* Generated by software containing ST-Developer
 * from STEP Tools, Inc. (www.steptools.com) 
 */

FILE_DESCRIPTION(
/* description */ ('Cam-driven reciprocating slide'),
/* implementation_level */ '2;1');

FILE_NAME(
/* name */ 'Bearing cap (2).step',
/* time_stamp */ '2026-10-28T03:25:20-07:00',
/* author */ (''),
/* organization */ (''),
/* preprocessor_version */ 'ST-DEVELOPER v20.2',
/* originating_system */ 'Autodesk Translation Framework v15.17.0.0',
/* authorisation */ '');

FILE_SCHEMA (('AUTOMOTIVE_DESIGN { 1 0 10303 214 3 1 1 }'));
ENDSEC;

DATA;
#10=MECHANICAL_DESIGN_GEOMETRIC_PRESENTATION_REPRESENTATION('',(#429),#13277);
#355=SHAPE_REPRESENTATION_RELATIONSHIP('SRR','None',#13448,#392);
#392=ADVANCED_BREP_SHAPE_REPRESENTATION('',(#473),#13243);
#429=STYLED_ITEM('',(#13720),#473);
#473=MANIFOLD_SOLID_BREP('Body1',#6405);
#570=FACE_BOUND('',#1432,.T.);
#571=FACE_BOUND('',#1436,.T.);
#572=FACE_BOUND('',#1437,.T.);
#573=FACE_BOUND('',#1438,.T.);
#574=FACE_BOUND('',#1439,.T.);
#575=FACE_BOUND('',#1440,.T.);
#576=FACE_BOUND('',#1442,.T.);
#577=FACE_BOUND('',#1443,.T.);
#578=FACE_BOUND('',#1444,.T.);
#579=FACE_BOUND('',#1445,.T.);
#580=FACE_BOUND('',#1446,.T.);
#730=PLANE('',#7029);
#731=PLANE('',#7036);
#732=PLANE('',#7037);
#984=FACE_OUTER_BOUND('',#1426,.T.);
#985=FACE_OUTER_BOUND('',#1427,.T.);
#986=FACE_OUTER_BOUND('',#1428,.T.);
#987=FACE_OUTER_BOUND('',#1429,.T.);
#988=FACE_OUTER_BOUND('',#1430,.T.);
#989=FACE_OUTER_BOUND('',#1431,.T.);
#990=FACE_OUTER_BOUND('',#1433,.T.);
#991=FACE_OUTER_BOUND('',#1434,.T.);
#992=FACE_OUTER_BOUND('',#1435,.T.);
#993=FACE_OUTER_BOUND('',#1441,.T.);
#1426=EDGE_LOOP('',(#4732,#4733,#4734,#4735));
#1427=EDGE_LOOP('',(#4736,#4737,#4738,#4739));
#1428=EDGE_LOOP('',(#4740,#4741,#4742,#4743));
#1429=EDGE_LOOP('',(#4744,#4745,#4746,#4747));
#1430=EDGE_LOOP('',(#4748,#4749,#4750,#4751));
#1431=EDGE_LOOP('',(#4752));
#1432=EDGE_LOOP('',(#4753));
#1433=EDGE_LOOP('',(#4754,#4755,#4756,#4757));
#1434=EDGE_LOOP('',(#4758,#4759,#4760,#4761));
#1435=EDGE_LOOP('',(#4762));
#1436=EDGE_LOOP('',(#4763));
#1437=EDGE_LOOP('',(#4764));
#1438=EDGE_LOOP('',(#4765));
#1439=EDGE_LOOP('',(#4766));
#1440=EDGE_LOOP('',(#4767));
#1441=EDGE_LOOP('',(#4768));
#1442=EDGE_LOOP('',(#4769));
#1443=EDGE_LOOP('',(#4770));
#1444=EDGE_LOOP('',(#4771));
#1445=EDGE_LOOP('',(#4772));
#1446=EDGE_LOOP('',(#4773));
#1963=LINE('',#10167,#2402);
#1964=LINE('',#10173,#2403);
#1965=LINE('',#10179,#2404);
#1966=LINE('',#10185,#2405);
#1967=LINE('',#10191,#2406);
#1968=LINE('',#10198,#2407);
#1969=LINE('',#10204,#2408);
#2402=VECTOR('',#8125,0.225);
#2403=VECTOR('',#8132,0.225);
#2404=VECTOR('',#8139,0.225);
#2405=VECTOR('',#8146,0.225);
#2406=VECTOR('',#8153,1.59);
#2407=VECTOR('',#8162,1.005);
#2408=VECTOR('',#8169,2.4);
#2779=CIRCLE('',#7015,0.225);
#2780=CIRCLE('',#7016,0.225);
#2781=CIRCLE('',#7018,0.225);
#2782=CIRCLE('',#7019,0.225);
#2783=CIRCLE('',#7021,0.225);
#2784=CIRCLE('',#7022,0.225);
#2785=CIRCLE('',#7024,0.225);
#2786=CIRCLE('',#7025,0.225);
#2787=CIRCLE('',#7027,1.59);
#2788=CIRCLE('',#7028,1.59);
#2789=CIRCLE('',#7030,1.005);
#2790=CIRCLE('',#7032,1.005);
#2791=CIRCLE('',#7034,2.4);
#2792=CIRCLE('',#7035,2.4);
#3167=VERTEX_POINT('',#10164);
#3168=VERTEX_POINT('',#10166);
#3169=VERTEX_POINT('',#10170);
#3170=VERTEX_POINT('',#10172);
#3171=VERTEX_POINT('',#10176);
#3172=VERTEX_POINT('',#10178);
#3173=VERTEX_POINT('',#10182);
#3174=VERTEX_POINT('',#10184);
#3175=VERTEX_POINT('',#10188);
#3176=VERTEX_POINT('',#10190);
#3177=VERTEX_POINT('',#10194);
#3178=VERTEX_POINT('',#10197);
#3179=VERTEX_POINT('',#10201);
#3180=VERTEX_POINT('',#10203);
#3756=EDGE_CURVE('',#3167,#3167,#2779,.T.);
#3757=EDGE_CURVE('',#3167,#3168,#1963,.T.);
#3758=EDGE_CURVE('',#3168,#3168,#2780,.T.);
#3759=EDGE_CURVE('',#3169,#3169,#2781,.T.);
#3760=EDGE_CURVE('',#3169,#3170,#1964,.T.);
#3761=EDGE_CURVE('',#3170,#3170,#2782,.T.);
#3762=EDGE_CURVE('',#3171,#3171,#2783,.T.);
#3763=EDGE_CURVE('',#3171,#3172,#1965,.T.);
#3764=EDGE_CURVE('',#3172,#3172,#2784,.T.);
#3765=EDGE_CURVE('',#3173,#3173,#2785,.T.);
#3766=EDGE_CURVE('',#3173,#3174,#1966,.T.);
#3767=EDGE_CURVE('',#3174,#3174,#2786,.T.);
#3768=EDGE_CURVE('',#3175,#3175,#2787,.T.);
#3769=EDGE_CURVE('',#3175,#3176,#1967,.T.);
#3770=EDGE_CURVE('',#3176,#3176,#2788,.T.);
#3771=EDGE_CURVE('',#3177,#3177,#2789,.T.);
#3772=EDGE_CURVE('',#3177,#3178,#1968,.T.);
#3773=EDGE_CURVE('',#3178,#3178,#2790,.T.);
#3774=EDGE_CURVE('',#3179,#3179,#2791,.T.);
#3775=EDGE_CURVE('',#3179,#3180,#1969,.T.);
#3776=EDGE_CURVE('',#3180,#3180,#2792,.T.);
#4732=ORIENTED_EDGE('',*,*,#3756,.F.);
#4733=ORIENTED_EDGE('',*,*,#3757,.T.);
#4734=ORIENTED_EDGE('',*,*,#3758,.F.);
#4735=ORIENTED_EDGE('',*,*,#3757,.F.);
#4736=ORIENTED_EDGE('',*,*,#3759,.F.);
#4737=ORIENTED_EDGE('',*,*,#3760,.T.);
#4738=ORIENTED_EDGE('',*,*,#3761,.F.);
#4739=ORIENTED_EDGE('',*,*,#3760,.F.);
#4740=ORIENTED_EDGE('',*,*,#3762,.F.);
#4741=ORIENTED_EDGE('',*,*,#3763,.T.);
#4742=ORIENTED_EDGE('',*,*,#3764,.F.);
#4743=ORIENTED_EDGE('',*,*,#3763,.F.);
#4744=ORIENTED_EDGE('',*,*,#3765,.F.);
#4745=ORIENTED_EDGE('',*,*,#3766,.T.);
#4746=ORIENTED_EDGE('',*,*,#3767,.F.);
#4747=ORIENTED_EDGE('',*,*,#3766,.F.);
#4748=ORIENTED_EDGE('',*,*,#3768,.F.);
#4749=ORIENTED_EDGE('',*,*,#3769,.T.);
#4750=ORIENTED_EDGE('',*,*,#3770,.F.);
#4751=ORIENTED_EDGE('',*,*,#3769,.F.);
#4752=ORIENTED_EDGE('',*,*,#3768,.T.);
#4753=ORIENTED_EDGE('',*,*,#3771,.T.);
#4754=ORIENTED_EDGE('',*,*,#3771,.F.);
#4755=ORIENTED_EDGE('',*,*,#3772,.T.);
#4756=ORIENTED_EDGE('',*,*,#3773,.T.);
#4757=ORIENTED_EDGE('',*,*,#3772,.F.);
#4758=ORIENTED_EDGE('',*,*,#3774,.F.);
#4759=ORIENTED_EDGE('',*,*,#3775,.T.);
#4760=ORIENTED_EDGE('',*,*,#3776,.T.);
#4761=ORIENTED_EDGE('',*,*,#3775,.F.);
#4762=ORIENTED_EDGE('',*,*,#3774,.T.);
#4763=ORIENTED_EDGE('',*,*,#3770,.T.);
#4764=ORIENTED_EDGE('',*,*,#3767,.T.);
#4765=ORIENTED_EDGE('',*,*,#3764,.T.);
#4766=ORIENTED_EDGE('',*,*,#3761,.T.);
#4767=ORIENTED_EDGE('',*,*,#3758,.T.);
#4768=ORIENTED_EDGE('',*,*,#3776,.F.);
#4769=ORIENTED_EDGE('',*,*,#3773,.F.);
#4770=ORIENTED_EDGE('',*,*,#3765,.T.);
#4771=ORIENTED_EDGE('',*,*,#3762,.T.);
#4772=ORIENTED_EDGE('',*,*,#3759,.T.);
#4773=ORIENTED_EDGE('',*,*,#3756,.T.);
#5926=CYLINDRICAL_SURFACE('',#7014,0.225);
#5927=CYLINDRICAL_SURFACE('',#7017,0.225);
#5928=CYLINDRICAL_SURFACE('',#7020,0.225);
#5929=CYLINDRICAL_SURFACE('',#7023,0.225);
#5930=CYLINDRICAL_SURFACE('',#7026,1.59);
#5931=CYLINDRICAL_SURFACE('',#7031,1.005);
#5932=CYLINDRICAL_SURFACE('',#7033,2.4);
#6102=ADVANCED_FACE('',(#984),#5926,.F.);
#6103=ADVANCED_FACE('',(#985),#5927,.F.);
#6104=ADVANCED_FACE('',(#986),#5928,.F.);
#6105=ADVANCED_FACE('',(#987),#5929,.F.);
#6106=ADVANCED_FACE('',(#988),#5930,.T.);
#6107=ADVANCED_FACE('',(#989,#570),#730,.T.);
#6108=ADVANCED_FACE('',(#990),#5931,.F.);
#6109=ADVANCED_FACE('',(#991),#5932,.T.);
#6110=ADVANCED_FACE('',(#992,#571,#572,#573,#574,#575),#731,.T.);
#6111=ADVANCED_FACE('',(#993,#576,#577,#578,#579,#580),#732,.F.);
#6405=CLOSED_SHELL('',(#6102,#6103,#6104,#6105,#6106,#6107,#6108,#6109,
#6110,#6111));
#7013=AXIS2_PLACEMENT_3D('',#10162,#8119,#8120);
#7014=AXIS2_PLACEMENT_3D('',#10163,#8121,#8122);
#7015=AXIS2_PLACEMENT_3D('',#10165,#8123,#8124);
#7016=AXIS2_PLACEMENT_3D('',#10168,#8126,#8127);
#7017=AXIS2_PLACEMENT_3D('',#10169,#8128,#8129);
#7018=AXIS2_PLACEMENT_3D('',#10171,#8130,#8131);
#7019=AXIS2_PLACEMENT_3D('',#10174,#8133,#8134);
#7020=AXIS2_PLACEMENT_3D('',#10175,#8135,#8136);
#7021=AXIS2_PLACEMENT_3D('',#10177,#8137,#8138);
#7022=AXIS2_PLACEMENT_3D('',#10180,#8140,#8141);
#7023=AXIS2_PLACEMENT_3D('',#10181,#8142,#8143);
#7024=AXIS2_PLACEMENT_3D('',#10183,#8144,#8145);
#7025=AXIS2_PLACEMENT_3D('',#10186,#8147,#8148);
#7026=AXIS2_PLACEMENT_3D('',#10187,#8149,#8150);
#7027=AXIS2_PLACEMENT_3D('',#10189,#8151,#8152);
#7028=AXIS2_PLACEMENT_3D('',#10192,#8154,#8155);
#7029=AXIS2_PLACEMENT_3D('',#10193,#8156,#8157);
#7030=AXIS2_PLACEMENT_3D('',#10195,#8158,#8159);
#7031=AXIS2_PLACEMENT_3D('',#10196,#8160,#8161);
#7032=AXIS2_PLACEMENT_3D('',#10199,#8163,#8164);
#7033=AXIS2_PLACEMENT_3D('',#10200,#8165,#8166);
#7034=AXIS2_PLACEMENT_3D('',#10202,#8167,#8168);
#7035=AXIS2_PLACEMENT_3D('',#10205,#8170,#8171);
#7036=AXIS2_PLACEMENT_3D('',#10206,#8172,#8173);
#7037=AXIS2_PLACEMENT_3D('',#10207,#8174,#8175);
#8119=DIRECTION('axis',(0.,0.,1.));
#8120=DIRECTION('refdir',(1.,0.,0.));
#8121=DIRECTION('center_axis',(0.,1.,0.));
#8122=DIRECTION('ref_axis',(1.,0.,0.));
#8123=DIRECTION('center_axis',(0.,1.,0.));
#8124=DIRECTION('ref_axis',(1.,0.,0.));
#8125=DIRECTION('',(0.,1.,0.));
#8126=DIRECTION('center_axis',(0.,-1.,0.));
#8127=DIRECTION('ref_axis',(1.,0.,0.));
#8128=DIRECTION('center_axis',(0.,1.,0.));
#8129=DIRECTION('ref_axis',(1.,0.,0.));
#8130=DIRECTION('center_axis',(0.,1.,0.));
#8131=DIRECTION('ref_axis',(1.,0.,0.));
#8132=DIRECTION('',(0.,1.,0.));
#8133=DIRECTION('center_axis',(0.,-1.,0.));
#8134=DIRECTION('ref_axis',(1.,0.,0.));
#8135=DIRECTION('center_axis',(0.,1.,0.));
#8136=DIRECTION('ref_axis',(1.,0.,0.));
#8137=DIRECTION('center_axis',(0.,1.,0.));
#8138=DIRECTION('ref_axis',(1.,0.,0.));
#8139=DIRECTION('',(0.,1.,0.));
#8140=DIRECTION('center_axis',(0.,-1.,0.));
#8141=DIRECTION('ref_axis',(1.,0.,0.));
#8142=DIRECTION('center_axis',(0.,1.,0.));
#8143=DIRECTION('ref_axis',(1.,0.,0.));
#8144=DIRECTION('center_axis',(0.,1.,0.));
#8145=DIRECTION('ref_axis',(1.,0.,0.));
#8146=DIRECTION('',(0.,1.,0.));
#8147=DIRECTION('center_axis',(0.,-1.,0.));
#8148=DIRECTION('ref_axis',(1.,0.,0.));
#8149=DIRECTION('center_axis',(0.,1.,0.));
#8150=DIRECTION('ref_axis',(1.,0.,0.));
#8151=DIRECTION('center_axis',(0.,1.,0.));
#8152=DIRECTION('ref_axis',(1.,0.,0.));
#8153=DIRECTION('',(0.,-1.,0.));
#8154=DIRECTION('center_axis',(0.,-1.,0.));
#8155=DIRECTION('ref_axis',(1.,0.,0.));
#8156=DIRECTION('center_axis',(0.,1.,0.));
#8157=DIRECTION('ref_axis',(1.,0.,0.));
#8158=DIRECTION('center_axis',(0.,-1.,0.));
#8159=DIRECTION('ref_axis',(1.,0.,0.));
#8160=DIRECTION('center_axis',(0.,1.,0.));
#8161=DIRECTION('ref_axis',(1.,0.,0.));
#8162=DIRECTION('',(0.,-1.,0.));
#8163=DIRECTION('center_axis',(0.,-1.,0.));
#8164=DIRECTION('ref_axis',(1.,0.,0.));
#8165=DIRECTION('center_axis',(0.,1.,0.));
#8166=DIRECTION('ref_axis',(1.,0.,0.));
#8167=DIRECTION('center_axis',(0.,1.,0.));
#8168=DIRECTION('ref_axis',(1.,0.,0.));
#8169=DIRECTION('',(0.,-1.,0.));
#8170=DIRECTION('center_axis',(0.,1.,0.));
#8171=DIRECTION('ref_axis',(1.,0.,0.));
#8172=DIRECTION('center_axis',(0.,1.,0.));
#8173=DIRECTION('ref_axis',(1.,0.,0.));
#8174=DIRECTION('center_axis',(0.,1.,0.));
#8175=DIRECTION('ref_axis',(1.,0.,0.));
#10162=CARTESIAN_POINT('',(0.,0.,0.));
#10163=CARTESIAN_POINT('Origin',(-1.4142135623731,1.4,2.58578643762691));
#10164=CARTESIAN_POINT('',(-1.6392135623731,1.5,2.58578643762691));
#10165=CARTESIAN_POINT('Origin',(-1.4142135623731,1.5,2.58578643762691));
#10166=CARTESIAN_POINT('',(-1.6392135623731,1.7,2.58578643762691));
#10167=CARTESIAN_POINT('',(-1.6392135623731,1.4,2.58578643762691));
#10168=CARTESIAN_POINT('Origin',(-1.4142135623731,1.7,2.58578643762691));
#10169=CARTESIAN_POINT('Origin',(-1.41421356237309,1.4,5.41421356237309));
#10170=CARTESIAN_POINT('',(-1.6392135623731,1.5,5.41421356237309));
#10171=CARTESIAN_POINT('Origin',(-1.41421356237309,1.5,5.41421356237309));
#10172=CARTESIAN_POINT('',(-1.6392135623731,1.7,5.41421356237309));
#10173=CARTESIAN_POINT('',(-1.6392135623731,1.4,5.41421356237309));
#10174=CARTESIAN_POINT('Origin',(-1.41421356237309,1.7,5.41421356237309));
#10175=CARTESIAN_POINT('Origin',(1.4142135623731,1.4,5.41421356237309));
#10176=CARTESIAN_POINT('',(1.1892135623731,1.5,5.41421356237309));
#10177=CARTESIAN_POINT('Origin',(1.4142135623731,1.5,5.41421356237309));
#10178=CARTESIAN_POINT('',(1.1892135623731,1.7,5.41421356237309));
#10179=CARTESIAN_POINT('',(1.1892135623731,1.4,5.41421356237309));
#10180=CARTESIAN_POINT('Origin',(1.4142135623731,1.7,5.41421356237309));
#10181=CARTESIAN_POINT('Origin',(1.41421356237309,1.4,2.5857864376269));
#10182=CARTESIAN_POINT('',(1.18921356237309,1.5,2.5857864376269));
#10183=CARTESIAN_POINT('Origin',(1.41421356237309,1.5,2.5857864376269));
#10184=CARTESIAN_POINT('',(1.18921356237309,1.7,2.5857864376269));
#10185=CARTESIAN_POINT('',(1.18921356237309,1.4,2.5857864376269));
#10186=CARTESIAN_POINT('Origin',(1.41421356237309,1.7,2.5857864376269));
#10187=CARTESIAN_POINT('Origin',(0.,1.7,4.));
#10188=CARTESIAN_POINT('',(-1.59,2.,4.));
#10189=CARTESIAN_POINT('Origin',(0.,2.,4.));
#10190=CARTESIAN_POINT('',(-1.59,1.7,4.));
#10191=CARTESIAN_POINT('',(-1.59,1.7,4.));
#10192=CARTESIAN_POINT('Origin',(0.,1.7,4.));
#10193=CARTESIAN_POINT('Origin',(0.,2.,4.));
#10194=CARTESIAN_POINT('',(-1.005,2.,4.));
#10195=CARTESIAN_POINT('Origin',(0.,2.,4.));
#10196=CARTESIAN_POINT('Origin',(0.,1.5,4.));
#10197=CARTESIAN_POINT('',(-1.005,1.5,4.));
#10198=CARTESIAN_POINT('',(-1.005,1.5,4.));
#10199=CARTESIAN_POINT('Origin',(0.,1.5,4.));
#10200=CARTESIAN_POINT('Origin',(0.,1.5,4.));
#10201=CARTESIAN_POINT('',(-2.4,1.7,4.));
#10202=CARTESIAN_POINT('Origin',(0.,1.7,4.));
#10203=CARTESIAN_POINT('',(-2.4,1.5,4.));
#10204=CARTESIAN_POINT('',(-2.4,1.5,4.));
#10205=CARTESIAN_POINT('Origin',(0.,1.5,4.));
#10206=CARTESIAN_POINT('Origin',(0.,1.7,4.));
#10207=CARTESIAN_POINT('Origin',(0.,1.5,4.));
#13199=UNCERTAINTY_MEASURE_WITH_UNIT(LENGTH_MEASURE(0.001),#13278,
'DISTANCE_ACCURACY_VALUE',
'Maximum model space distance between geometric entities at asserted c
onnectivities');
#13233=UNCERTAINTY_MEASURE_WITH_UNIT(LENGTH_MEASURE(0.001),#13278,
'DISTANCE_ACCURACY_VALUE',
'Maximum model space distance between geometric entities at asserted c
onnectivities');
#13243=(
GEOMETRIC_REPRESENTATION_CONTEXT(3)
GLOBAL_UNCERTAINTY_ASSIGNED_CONTEXT((#13199))
GLOBAL_UNIT_ASSIGNED_CONTEXT((#13278,#13280,#13281))
REPRESENTATION_CONTEXT('','3D')
);
#13277=(
GEOMETRIC_REPRESENTATION_CONTEXT(3)
GLOBAL_UNCERTAINTY_ASSIGNED_CONTEXT((#13233))
GLOBAL_UNIT_ASSIGNED_CONTEXT((#13278,#13280,#13281))
REPRESENTATION_CONTEXT('','3D')
);
#13278=(
LENGTH_UNIT()
NAMED_UNIT(*)
SI_UNIT(.CENTI.,.METRE.)
);
#13280=(
NAMED_UNIT(*)
PLANE_ANGLE_UNIT()
SI_UNIT($,.RADIAN.)
);
#13281=(
NAMED_UNIT(*)
SI_UNIT($,.STERADIAN.)
SOLID_ANGLE_UNIT()
);
#13291=SHAPE_DEFINITION_REPRESENTATION(#13334,#13448);
#13334=PRODUCT_DEFINITION_SHAPE('',$,#13492);
#13448=SHAPE_REPRESENTATION('',(#7013),#13243);
#13482=PRODUCT_DEFINITION_CONTEXT('part definition',#13613,'design');
#13492=PRODUCT_DEFINITION('Bearing cap (2)','Bearing cap (2)',#13535,#13482);
#13535=PRODUCT_DEFINITION_FORMATION('',$,#13624);
#13613=APPLICATION_CONTEXT(
'Core Data for Automotive Mechanical Design Process');
#13614=PRODUCT_CONTEXT('part definition',#13613,'mechanical');
#13624=PRODUCT('Bearing cap (2)','Bearing cap (2)','Bearing cap (2)',(#13614));
#13714=COLOUR_RGB('Grey',0.48,0.52,0.57);
#13715=FILL_AREA_STYLE_COLOUR('',#13714);
#13716=FILL_AREA_STYLE('',(#13715));
#13717=SURFACE_STYLE_FILL_AREA(#13716);
#13718=SURFACE_SIDE_STYLE('',(#13717));
#13719=SURFACE_STYLE_USAGE(.BOTH.,#13718);
#13720=PRESENTATION_STYLE_ASSIGNMENT((#13719));
ENDSEC;
END-ISO-10303-21;
